ISO-10303-21;
HEADER;
/* Generated by software containing ST-Developer
 * from STEP Tools, Inc. (www.steptools.com) 
 */

FILE_DESCRIPTION(
/* description */ ('Lifting hook block with sheave'),
/* implementation_level */ '2;1');

FILE_NAME(
/* name */ 'Eye spacer (1).step',
/* time_stamp */ '2026-10-28T03:23:54-07:00',
/* author */ (''),
/* organization */ (''),
/* preprocessor_version */ 'ST-DEVELOPER v20.2',
/* originating_system */ 'Autodesk Translation Framework v15.17.0.0',
/* authorisation */ '');

FILE_SCHEMA (('AUTOMOTIVE_DESIGN { 1 0 10303 214 3 1 1 }'));
ENDSEC;

DATA;
#10=MECHANICAL_DESIGN_GEOMETRIC_PRESENTATION_REPRESENTATION('',(#362),#9391);
#302=SHAPE_REPRESENTATION_RELATIONSHIP('SRR','None',#9533,#332);
#332=ADVANCED_BREP_SHAPE_REPRESENTATION('',(#400),#9368);
#362=STYLED_ITEM('',(#9745),#400);
#400=MANIFOLD_SOLID_BREP('Body1',#4898);
#538=LINE('',#8039,#826);
#539=LINE('',#8045,#827);
#826=VECTOR('',#6479,1.005);
#827=VECTOR('',#6486,1.4);
#1046=CYLINDRICAL_SURFACE('',#5475,1.005);
#1047=CYLINDRICAL_SURFACE('',#5478,1.4);
#1157=FACE_BOUND('',#1658,.T.);
#1158=FACE_BOUND('',#1660,.T.);
#1316=FACE_OUTER_BOUND('',#1655,.T.);
#1317=FACE_OUTER_BOUND('',#1656,.T.);
#1318=FACE_OUTER_BOUND('',#1657,.T.);
#1319=FACE_OUTER_BOUND('',#1659,.T.);
#1655=EDGE_LOOP('',(#3674,#3675,#3676,#3677));
#1656=EDGE_LOOP('',(#3678,#3679,#3680,#3681));
#1657=EDGE_LOOP('',(#3682));
#1658=EDGE_LOOP('',(#3683));
#1659=EDGE_LOOP('',(#3684));
#1660=EDGE_LOOP('',(#3685));
#2023=CIRCLE('',#5476,1.005);
#2024=CIRCLE('',#5477,1.005);
#2025=CIRCLE('',#5479,1.4);
#2026=CIRCLE('',#5480,1.4);
#2356=VERTEX_POINT('',#8036);
#2357=VERTEX_POINT('',#8038);
#2358=VERTEX_POINT('',#8042);
#2359=VERTEX_POINT('',#8044);
#2841=EDGE_CURVE('',#2356,#2356,#2023,.T.);
#2842=EDGE_CURVE('',#2356,#2357,#538,.T.);
#2843=EDGE_CURVE('',#2357,#2357,#2024,.T.);
#2844=EDGE_CURVE('',#2358,#2358,#2025,.T.);
#2845=EDGE_CURVE('',#2358,#2359,#539,.T.);
#2846=EDGE_CURVE('',#2359,#2359,#2026,.T.);
#3674=ORIENTED_EDGE('',*,*,#2841,.F.);
#3675=ORIENTED_EDGE('',*,*,#2842,.T.);
#3676=ORIENTED_EDGE('',*,*,#2843,.T.);
#3677=ORIENTED_EDGE('',*,*,#2842,.F.);
#3678=ORIENTED_EDGE('',*,*,#2844,.F.);
#3679=ORIENTED_EDGE('',*,*,#2845,.T.);
#3680=ORIENTED_EDGE('',*,*,#2846,.T.);
#3681=ORIENTED_EDGE('',*,*,#2845,.F.);
#3682=ORIENTED_EDGE('',*,*,#2844,.T.);
#3683=ORIENTED_EDGE('',*,*,#2841,.T.);
#3684=ORIENTED_EDGE('',*,*,#2846,.F.);
#3685=ORIENTED_EDGE('',*,*,#2843,.F.);
#4500=PLANE('',#5481);
#4501=PLANE('',#5482);
#4692=ADVANCED_FACE('',(#1316),#1046,.F.);
#4693=ADVANCED_FACE('',(#1317),#1047,.T.);
#4694=ADVANCED_FACE('',(#1318,#1157),#4500,.T.);
#4695=ADVANCED_FACE('',(#1319,#1158),#4501,.F.);
#4898=CLOSED_SHELL('',(#4692,#4693,#4694,#4695));
#5474=AXIS2_PLACEMENT_3D('',#8034,#6473,#6474);
#5475=AXIS2_PLACEMENT_3D('',#8035,#6475,#6476);
#5476=AXIS2_PLACEMENT_3D('',#8037,#6477,#6478);
#5477=AXIS2_PLACEMENT_3D('',#8040,#6480,#6481);
#5478=AXIS2_PLACEMENT_3D('',#8041,#6482,#6483);
#5479=AXIS2_PLACEMENT_3D('',#8043,#6484,#6485);
#5480=AXIS2_PLACEMENT_3D('',#8046,#6487,#6488);
#5481=AXIS2_PLACEMENT_3D('',#8047,#6489,#6490);
#5482=AXIS2_PLACEMENT_3D('',#8048,#6491,#6492);
#6473=DIRECTION('axis',(0.,0.,1.));
#6474=DIRECTION('refdir',(1.,0.,0.));
#6475=DIRECTION('center_axis',(0.,1.,0.));
#6476=DIRECTION('ref_axis',(1.,0.,0.));
#6477=DIRECTION('center_axis',(0.,-1.,0.));
#6478=DIRECTION('ref_axis',(1.,0.,0.));
#6479=DIRECTION('',(0.,-1.,0.));
#6480=DIRECTION('center_axis',(0.,-1.,0.));
#6481=DIRECTION('ref_axis',(1.,0.,0.));
#6482=DIRECTION('center_axis',(0.,1.,0.));
#6483=DIRECTION('ref_axis',(1.,0.,0.));
#6484=DIRECTION('center_axis',(0.,1.,0.));
#6485=DIRECTION('ref_axis',(1.,0.,0.));
#6486=DIRECTION('',(0.,-1.,0.));
#6487=DIRECTION('center_axis',(0.,1.,0.));
#6488=DIRECTION('ref_axis',(1.,0.,0.));
#6489=DIRECTION('center_axis',(0.,1.,0.));
#6490=DIRECTION('ref_axis',(1.,0.,0.));
#6491=DIRECTION('center_axis',(0.,1.,0.));
#6492=DIRECTION('ref_axis',(1.,0.,0.));
#8034=CARTESIAN_POINT('',(0.,0.,0.));
#8035=CARTESIAN_POINT('Origin',(0.,0.8,20.5));
#8036=CARTESIAN_POINT('',(-1.005,2.5,20.5));
#8037=CARTESIAN_POINT('Origin',(0.,2.5,20.5));
#8038=CARTESIAN_POINT('',(-1.005,0.8,20.5));
#8039=CARTESIAN_POINT('',(-1.005,0.8,20.5));
#8040=CARTESIAN_POINT('Origin',(0.,0.8,20.5));
#8041=CARTESIAN_POINT('Origin',(0.,0.8,20.5));
#8042=CARTESIAN_POINT('',(-1.4,2.5,20.5));
#8043=CARTESIAN_POINT('Origin',(0.,2.5,20.5));
#8044=CARTESIAN_POINT('',(-1.4,0.8,20.5));
#8045=CARTESIAN_POINT('',(-1.4,0.8,20.5));
#8046=CARTESIAN_POINT('Origin',(0.,0.8,20.5));
#8047=CARTESIAN_POINT('Origin',(0.,2.5,20.5));
#8048=CARTESIAN_POINT('Origin',(0.,0.8,20.5));
#9331=UNCERTAINTY_MEASURE_WITH_UNIT(LENGTH_MEASURE(0.001),#9392,
'DISTANCE_ACCURACY_VALUE',
'Maximum model space distance between geometric entities at asserted c
onnectivities');
#9354=UNCERTAINTY_MEASURE_WITH_UNIT(LENGTH_MEASURE(0.001),#9392,
'DISTANCE_ACCURACY_VALUE',
'Maximum model space distance between geometric entities at asserted c
onnectivities');
#9368=(
GEOMETRIC_REPRESENTATION_CONTEXT(3)
GLOBAL_UNCERTAINTY_ASSIGNED_CONTEXT((#9331))
GLOBAL_UNIT_ASSIGNED_CONTEXT((#9392,#9394,#9395))
REPRESENTATION_CONTEXT('','3D')
);
#9391=(
GEOMETRIC_REPRESENTATION_CONTEXT(3)
GLOBAL_UNCERTAINTY_ASSIGNED_CONTEXT((#9354))
GLOBAL_UNIT_ASSIGNED_CONTEXT((#9392,#9394,#9395))
REPRESENTATION_CONTEXT('','3D')
);
#9392=(
LENGTH_UNIT()
NAMED_UNIT(*)
SI_UNIT(.CENTI.,.METRE.)
);
#9394=(
NAMED_UNIT(*)
PLANE_ANGLE_UNIT()
SI_UNIT($,.RADIAN.)
);
#9395=(
NAMED_UNIT(*)
SI_UNIT($,.STERADIAN.)
SOLID_ANGLE_UNIT()
);
#9409=SHAPE_DEFINITION_REPRESENTATION(#9445,#9533);
#9445=PRODUCT_DEFINITION_SHAPE('',$,#9570);
#9533=SHAPE_REPRESENTATION('',(#5474),#9368);
#9556=PRODUCT_DEFINITION_CONTEXT('part definition',#9666,'design');
#9570=PRODUCT_DEFINITION('Eye spacer (1)','Eye spacer (1)',#9606,#9556);
#9606=PRODUCT_DEFINITION_FORMATION('',$,#9681);
#9666=APPLICATION_CONTEXT(
'Core Data for Automotive Mechanical Design Process');
#9667=PRODUCT_CONTEXT('part definition',#9666,'mechanical');
#9681=PRODUCT('Eye spacer (1)','Eye spacer (1)','Eye spacer (1)',(#9667));
#9739=COLOUR_RGB('Light Blue',0.38,0.62,0.78);
#9740=FILL_AREA_STYLE_COLOUR('',#9739);
#9741=FILL_AREA_STYLE('',(#9740));
#9742=SURFACE_STYLE_FILL_AREA(#9741);
#9743=SURFACE_SIDE_STYLE('',(#9742));
#9744=SURFACE_STYLE_USAGE(.BOTH.,#9743);
#9745=PRESENTATION_STYLE_ASSIGNMENT((#9744));
ENDSEC;
END-ISO-10303-21;
